ISO-10303-21;
HEADER;
/* Generated by software containing ST-Developer
 * from STEP Tools, Inc. (www.steptools.com) 
 */

FILE_DESCRIPTION(
/* description */ ('Four-wheel beam trolley'),
/* implementation_level */ '2;1');

FILE_NAME(
/* name */ 'M4x10 Cap Screw.step',
/* time_stamp */ '2026-10-29T16:22:06-07:00',
/* author */ (''),
/* organization */ (''),
/* preprocessor_version */ 'ST-DEVELOPER v20.2',
/* originating_system */ 'Autodesk Translation Framework v15.17.0.0',
/* authorisation */ '');

FILE_SCHEMA (('AUTOMOTIVE_DESIGN { 1 0 10303 214 3 1 1 }'));
ENDSEC;

DATA;
#10=MECHANICAL_DESIGN_GEOMETRIC_PRESENTATION_REPRESENTATION('',(#287),#4777);
#230=ORIENTED_CLOSED_SHELL('',*,#2375,.F.);
#235=CONICAL_SURFACE('',#2724,0.325,0.785398163397448);
#236=CONICAL_SURFACE('',#2728,0.335,0.785398163397448);
#237=CONICAL_SURFACE('',#2732,0.21,0.463647609000806);
#243=BREP_WITH_VOIDS('Body1',#2376,(#230));
#253=SHAPE_REPRESENTATION_RELATIONSHIP('SRR','None',#4882,#270);
#270=ADVANCED_BREP_SHAPE_REPRESENTATION('',(#243),#4767);
#287=STYLED_ITEM('',(#5063),#243);
#349=FACE_BOUND('',#699,.T.);
#409=PLANE('',#2712);
#410=PLANE('',#2713);
#411=PLANE('',#2714);
#412=PLANE('',#2715);
#413=PLANE('',#2716);
#414=PLANE('',#2717);
#415=PLANE('',#2718);
#416=PLANE('',#2719);
#417=PLANE('',#2720);
#418=PLANE('',#2722);
#419=PLANE('',#2730);
#513=FACE_OUTER_BOUND('',#685,.T.);
#514=FACE_OUTER_BOUND('',#686,.T.);
#515=FACE_OUTER_BOUND('',#687,.T.);
#516=FACE_OUTER_BOUND('',#688,.T.);
#517=FACE_OUTER_BOUND('',#689,.T.);
#518=FACE_OUTER_BOUND('',#690,.T.);
#519=FACE_OUTER_BOUND('',#691,.T.);
#520=FACE_OUTER_BOUND('',#692,.T.);
#521=FACE_OUTER_BOUND('',#693,.T.);
#522=FACE_OUTER_BOUND('',#694,.T.);
#523=FACE_OUTER_BOUND('',#695,.T.);
#524=FACE_OUTER_BOUND('',#696,.T.);
#525=FACE_OUTER_BOUND('',#697,.T.);
#526=FACE_OUTER_BOUND('',#698,.T.);
#527=FACE_OUTER_BOUND('',#700,.T.);
#528=FACE_OUTER_BOUND('',#701,.T.);
#685=EDGE_LOOP('',(#1881,#1882,#1883,#1884));
#686=EDGE_LOOP('',(#1885,#1886,#1887,#1888));
#687=EDGE_LOOP('',(#1889,#1890,#1891,#1892));
#688=EDGE_LOOP('',(#1893,#1894,#1895,#1896));
#689=EDGE_LOOP('',(#1897,#1898,#1899,#1900));
#690=EDGE_LOOP('',(#1901,#1902,#1903,#1904));
#691=EDGE_LOOP('',(#1905,#1906,#1907,#1908,#1909,#1910));
#692=EDGE_LOOP('',(#1911,#1912,#1913,#1914,#1915,#1916));
#693=EDGE_LOOP('',(#1917));
#694=EDGE_LOOP('',(#1918));
#695=EDGE_LOOP('',(#1919,#1920,#1921,#1922));
#696=EDGE_LOOP('',(#1923,#1924,#1925,#1926));
#697=EDGE_LOOP('',(#1927,#1928,#1929,#1930));
#698=EDGE_LOOP('',(#1931));
#699=EDGE_LOOP('',(#1932));
#700=EDGE_LOOP('',(#1933,#1934,#1935,#1936));
#701=EDGE_LOOP('',(#1937,#1938,#1939,#1940));
#855=LINE('',#4059,#978);
#856=LINE('',#4061,#979);
#857=LINE('',#4063,#980);
#858=LINE('',#4064,#981);
#859=LINE('',#4067,#982);
#860=LINE('',#4069,#983);
#861=LINE('',#4070,#984);
#862=LINE('',#4073,#985);
#863=LINE('',#4075,#986);
#864=LINE('',#4076,#987);
#865=LINE('',#4079,#988);
#866=LINE('',#4081,#989);
#867=LINE('',#4082,#990);
#868=LINE('',#4085,#991);
#869=LINE('',#4087,#992);
#870=LINE('',#4088,#993);
#871=LINE('',#4090,#994);
#872=LINE('',#4091,#995);
#873=LINE('',#4103,#996);
#874=LINE('',#4107,#997);
#875=LINE('',#4111,#998);
#876=LINE('',#4118,#999);
#877=LINE('',#4120,#1000);
#978=VECTOR('',#3278,1.);
#979=VECTOR('',#3279,1.);
#980=VECTOR('',#3280,1.);
#981=VECTOR('',#3281,1.);
#982=VECTOR('',#3284,1.);
#983=VECTOR('',#3285,1.);
#984=VECTOR('',#3286,1.);
#985=VECTOR('',#3289,1.);
#986=VECTOR('',#3290,1.);
#987=VECTOR('',#3291,1.);
#988=VECTOR('',#3294,1.);
#989=VECTOR('',#3295,1.);
#990=VECTOR('',#3296,1.);
#991=VECTOR('',#3299,1.);
#992=VECTOR('',#3300,1.);
#993=VECTOR('',#3301,1.);
#994=VECTOR('',#3304,1.);
#995=VECTOR('',#3305,1.);
#996=VECTOR('',#3322,0.325);
#997=VECTOR('',#3327,0.35);
#998=VECTOR('',#3332,0.335);
#999=VECTOR('',#3341,0.21);
#1000=VECTOR('',#3344,0.2);
#1073=CIRCLE('',#2721,0.1954);
#1074=CIRCLE('',#2723,0.3);
#1075=CIRCLE('',#2725,0.35);
#1076=CIRCLE('',#2727,0.35);
#1077=CIRCLE('',#2729,0.32);
#1078=CIRCLE('',#2731,0.22);
#1079=CIRCLE('',#2733,0.1954);
#1245=VERTEX_POINT('',#4057);
#1246=VERTEX_POINT('',#4058);
#1247=VERTEX_POINT('',#4060);
#1248=VERTEX_POINT('',#4062);
#1249=VERTEX_POINT('',#4066);
#1250=VERTEX_POINT('',#4068);
#1251=VERTEX_POINT('',#4072);
#1252=VERTEX_POINT('',#4074);
#1253=VERTEX_POINT('',#4078);
#1254=VERTEX_POINT('',#4080);
#1255=VERTEX_POINT('',#4084);
#1256=VERTEX_POINT('',#4086);
#1257=VERTEX_POINT('',#4095);
#1258=VERTEX_POINT('',#4098);
#1259=VERTEX_POINT('',#4101);
#1260=VERTEX_POINT('',#4105);
#1261=VERTEX_POINT('',#4109);
#1262=VERTEX_POINT('',#4113);
#1263=VERTEX_POINT('',#4116);
#1478=EDGE_CURVE('',#1245,#1246,#855,.T.);
#1479=EDGE_CURVE('',#1246,#1247,#856,.T.);
#1480=EDGE_CURVE('',#1247,#1248,#857,.T.);
#1481=EDGE_CURVE('',#1245,#1248,#858,.T.);
#1482=EDGE_CURVE('',#1246,#1249,#859,.T.);
#1483=EDGE_CURVE('',#1249,#1250,#860,.T.);
#1484=EDGE_CURVE('',#1250,#1247,#861,.T.);
#1485=EDGE_CURVE('',#1249,#1251,#862,.T.);
#1486=EDGE_CURVE('',#1251,#1252,#863,.T.);
#1487=EDGE_CURVE('',#1252,#1250,#864,.T.);
#1488=EDGE_CURVE('',#1251,#1253,#865,.T.);
#1489=EDGE_CURVE('',#1253,#1254,#866,.T.);
#1490=EDGE_CURVE('',#1254,#1252,#867,.T.);
#1491=EDGE_CURVE('',#1253,#1255,#868,.T.);
#1492=EDGE_CURVE('',#1255,#1256,#869,.T.);
#1493=EDGE_CURVE('',#1256,#1254,#870,.T.);
#1494=EDGE_CURVE('',#1255,#1245,#871,.T.);
#1495=EDGE_CURVE('',#1248,#1256,#872,.T.);
#1496=EDGE_CURVE('',#1257,#1257,#1073,.T.);
#1497=EDGE_CURVE('',#1258,#1258,#1074,.T.);
#1498=EDGE_CURVE('',#1259,#1259,#1075,.T.);
#1499=EDGE_CURVE('',#1259,#1258,#873,.T.);
#1500=EDGE_CURVE('',#1260,#1260,#1076,.T.);
#1501=EDGE_CURVE('',#1260,#1259,#874,.T.);
#1502=EDGE_CURVE('',#1261,#1261,#1077,.T.);
#1503=EDGE_CURVE('',#1261,#1260,#875,.T.);
#1504=EDGE_CURVE('',#1262,#1262,#1078,.T.);
#1505=EDGE_CURVE('',#1263,#1263,#1079,.F.);
#1506=EDGE_CURVE('',#1263,#1262,#876,.T.);
#1507=EDGE_CURVE('',#1257,#1263,#877,.T.);
#1881=ORIENTED_EDGE('',*,*,#1478,.T.);
#1882=ORIENTED_EDGE('',*,*,#1479,.T.);
#1883=ORIENTED_EDGE('',*,*,#1480,.T.);
#1884=ORIENTED_EDGE('',*,*,#1481,.F.);
#1885=ORIENTED_EDGE('',*,*,#1482,.T.);
#1886=ORIENTED_EDGE('',*,*,#1483,.T.);
#1887=ORIENTED_EDGE('',*,*,#1484,.T.);
#1888=ORIENTED_EDGE('',*,*,#1479,.F.);
#1889=ORIENTED_EDGE('',*,*,#1485,.T.);
#1890=ORIENTED_EDGE('',*,*,#1486,.T.);
#1891=ORIENTED_EDGE('',*,*,#1487,.T.);
#1892=ORIENTED_EDGE('',*,*,#1483,.F.);
#1893=ORIENTED_EDGE('',*,*,#1488,.T.);
#1894=ORIENTED_EDGE('',*,*,#1489,.T.);
#1895=ORIENTED_EDGE('',*,*,#1490,.T.);
#1896=ORIENTED_EDGE('',*,*,#1486,.F.);
#1897=ORIENTED_EDGE('',*,*,#1491,.T.);
#1898=ORIENTED_EDGE('',*,*,#1492,.T.);
#1899=ORIENTED_EDGE('',*,*,#1493,.T.);
#1900=ORIENTED_EDGE('',*,*,#1489,.F.);
#1901=ORIENTED_EDGE('',*,*,#1494,.T.);
#1902=ORIENTED_EDGE('',*,*,#1481,.T.);
#1903=ORIENTED_EDGE('',*,*,#1495,.T.);
#1904=ORIENTED_EDGE('',*,*,#1492,.F.);
#1905=ORIENTED_EDGE('',*,*,#1494,.F.);
#1906=ORIENTED_EDGE('',*,*,#1491,.F.);
#1907=ORIENTED_EDGE('',*,*,#1488,.F.);
#1908=ORIENTED_EDGE('',*,*,#1485,.F.);
#1909=ORIENTED_EDGE('',*,*,#1482,.F.);
#1910=ORIENTED_EDGE('',*,*,#1478,.F.);
#1911=ORIENTED_EDGE('',*,*,#1495,.F.);
#1912=ORIENTED_EDGE('',*,*,#1480,.F.);
#1913=ORIENTED_EDGE('',*,*,#1484,.F.);
#1914=ORIENTED_EDGE('',*,*,#1487,.F.);
#1915=ORIENTED_EDGE('',*,*,#1490,.F.);
#1916=ORIENTED_EDGE('',*,*,#1493,.F.);
#1917=ORIENTED_EDGE('',*,*,#1496,.F.);
#1918=ORIENTED_EDGE('',*,*,#1497,.F.);
#1919=ORIENTED_EDGE('',*,*,#1498,.F.);
#1920=ORIENTED_EDGE('',*,*,#1499,.T.);
#1921=ORIENTED_EDGE('',*,*,#1497,.T.);
#1922=ORIENTED_EDGE('',*,*,#1499,.F.);
#1923=ORIENTED_EDGE('',*,*,#1500,.F.);
#1924=ORIENTED_EDGE('',*,*,#1501,.T.);
#1925=ORIENTED_EDGE('',*,*,#1498,.T.);
#1926=ORIENTED_EDGE('',*,*,#1501,.F.);
#1927=ORIENTED_EDGE('',*,*,#1502,.F.);
#1928=ORIENTED_EDGE('',*,*,#1503,.T.);
#1929=ORIENTED_EDGE('',*,*,#1500,.T.);
#1930=ORIENTED_EDGE('',*,*,#1503,.F.);
#1931=ORIENTED_EDGE('',*,*,#1502,.T.);
#1932=ORIENTED_EDGE('',*,*,#1504,.F.);
#1933=ORIENTED_EDGE('',*,*,#1505,.F.);
#1934=ORIENTED_EDGE('',*,*,#1506,.T.);
#1935=ORIENTED_EDGE('',*,*,#1504,.T.);
#1936=ORIENTED_EDGE('',*,*,#1506,.F.);
#1937=ORIENTED_EDGE('',*,*,#1496,.T.);
#1938=ORIENTED_EDGE('',*,*,#1507,.T.);
#1939=ORIENTED_EDGE('',*,*,#1505,.T.);
#1940=ORIENTED_EDGE('',*,*,#1507,.F.);
#2198=CYLINDRICAL_SURFACE('',#2726,0.35);
#2199=CYLINDRICAL_SURFACE('',#2734,0.1954);
#2289=ADVANCED_FACE('',(#513),#409,.F.);
#2290=ADVANCED_FACE('',(#514),#410,.F.);
#2291=ADVANCED_FACE('',(#515),#411,.F.);
#2292=ADVANCED_FACE('',(#516),#412,.F.);
#2293=ADVANCED_FACE('',(#517),#413,.F.);
#2294=ADVANCED_FACE('',(#518),#414,.F.);
#2295=ADVANCED_FACE('',(#519),#415,.F.);
#2296=ADVANCED_FACE('',(#520),#416,.F.);
#2297=ADVANCED_FACE('',(#521),#417,.F.);
#2298=ADVANCED_FACE('',(#522),#418,.T.);
#2299=ADVANCED_FACE('',(#523),#235,.T.);
#2300=ADVANCED_FACE('',(#524),#2198,.T.);
#2301=ADVANCED_FACE('',(#525),#236,.T.);
#2302=ADVANCED_FACE('',(#526,#349),#419,.T.);
#2303=ADVANCED_FACE('',(#527),#237,.T.);
#2304=ADVANCED_FACE('',(#528),#2199,.T.);
#2375=CLOSED_SHELL('',(#2289,#2290,#2291,#2292,#2293,#2294,#2295,#2296));
#2376=CLOSED_SHELL('',(#2297,#2298,#2299,#2300,#2301,#2302,#2303,#2304));
#2711=AXIS2_PLACEMENT_3D('',#4055,#3274,#3275);
#2712=AXIS2_PLACEMENT_3D('',#4056,#3276,#3277);
#2713=AXIS2_PLACEMENT_3D('',#4065,#3282,#3283);
#2714=AXIS2_PLACEMENT_3D('',#4071,#3287,#3288);
#2715=AXIS2_PLACEMENT_3D('',#4077,#3292,#3293);
#2716=AXIS2_PLACEMENT_3D('',#4083,#3297,#3298);
#2717=AXIS2_PLACEMENT_3D('',#4089,#3302,#3303);
#2718=AXIS2_PLACEMENT_3D('',#4092,#3306,#3307);
#2719=AXIS2_PLACEMENT_3D('',#4093,#3308,#3309);
#2720=AXIS2_PLACEMENT_3D('',#4094,#3310,#3311);
#2721=AXIS2_PLACEMENT_3D('',#4096,#3312,#3313);
#2722=AXIS2_PLACEMENT_3D('',#4097,#3314,#3315);
#2723=AXIS2_PLACEMENT_3D('',#4099,#3316,#3317);
#2724=AXIS2_PLACEMENT_3D('',#4100,#3318,#3319);
#2725=AXIS2_PLACEMENT_3D('',#4102,#3320,#3321);
#2726=AXIS2_PLACEMENT_3D('',#4104,#3323,#3324);
#2727=AXIS2_PLACEMENT_3D('',#4106,#3325,#3326);
#2728=AXIS2_PLACEMENT_3D('',#4108,#3328,#3329);
#2729=AXIS2_PLACEMENT_3D('',#4110,#3330,#3331);
#2730=AXIS2_PLACEMENT_3D('',#4112,#3333,#3334);
#2731=AXIS2_PLACEMENT_3D('',#4114,#3335,#3336);
#2732=AXIS2_PLACEMENT_3D('',#4115,#3337,#3338);
#2733=AXIS2_PLACEMENT_3D('',#4117,#3339,#3340);
#2734=AXIS2_PLACEMENT_3D('',#4119,#3342,#3343);
#3274=DIRECTION('axis',(0.,0.,1.));
#3275=DIRECTION('refdir',(1.,0.,0.));
#3276=DIRECTION('center_axis',(0.866025403784439,0.,-0.5));
#3277=DIRECTION('ref_axis',(0.5,0.,0.866025403784439));
#3278=DIRECTION('',(-0.5,0.,-0.866025403784439));
#3279=DIRECTION('',(0.,-1.,0.));
#3280=DIRECTION('',(0.5,0.,0.866025403784439));
#3281=DIRECTION('',(0.,-1.,0.));
#3282=DIRECTION('center_axis',(1.60246890531964E-16,0.,-1.));
#3283=DIRECTION('ref_axis',(1.,0.,1.60246890531964E-16));
#3284=DIRECTION('',(-1.,0.,-1.60246890531964E-16));
#3285=DIRECTION('',(0.,-1.,0.));
#3286=DIRECTION('',(1.,0.,1.60246890531964E-16));
#3287=DIRECTION('center_axis',(-0.866025403784439,0.,-0.5));
#3288=DIRECTION('ref_axis',(0.5,0.,-0.866025403784439));
#3289=DIRECTION('',(-0.5,0.,0.866025403784439));
#3290=DIRECTION('',(0.,-1.,0.));
#3291=DIRECTION('',(0.5,0.,-0.866025403784439));
#3292=DIRECTION('center_axis',(-0.866025403784439,0.,0.5));
#3293=DIRECTION('ref_axis',(-0.5,0.,-0.866025403784439));
#3294=DIRECTION('',(0.5,0.,0.866025403784439));
#3295=DIRECTION('',(0.,-1.,0.));
#3296=DIRECTION('',(-0.5,0.,-0.866025403784439));
#3297=DIRECTION('center_axis',(-1.60246890531964E-16,0.,1.));
#3298=DIRECTION('ref_axis',(-1.,0.,-1.60246890531964E-16));
#3299=DIRECTION('',(1.,0.,1.60246890531964E-16));
#3300=DIRECTION('',(0.,-1.,0.));
#3301=DIRECTION('',(-1.,0.,-1.60246890531964E-16));
#3302=DIRECTION('center_axis',(0.866025403784439,0.,0.5));
#3303=DIRECTION('ref_axis',(-0.5,0.,0.866025403784439));
#3304=DIRECTION('',(0.5,0.,-0.866025403784439));
#3305=DIRECTION('',(-0.5,0.,0.866025403784439));
#3306=DIRECTION('center_axis',(0.,1.,0.));
#3307=DIRECTION('ref_axis',(1.,0.,0.));
#3308=DIRECTION('center_axis',(0.,-1.,0.));
#3309=DIRECTION('ref_axis',(0.,0.,-1.));
#3310=DIRECTION('center_axis',(0.,1.,0.));
#3311=DIRECTION('ref_axis',(1.,0.,0.));
#3312=DIRECTION('center_axis',(0.,1.,0.));
#3313=DIRECTION('ref_axis',(1.,0.,0.));
#3314=DIRECTION('center_axis',(0.,1.,0.));
#3315=DIRECTION('ref_axis',(0.,0.,1.));
#3316=DIRECTION('center_axis',(0.,-1.,0.));
#3317=DIRECTION('ref_axis',(1.,0.,0.));
#3318=DIRECTION('center_axis',(0.,-1.,0.));
#3319=DIRECTION('ref_axis',(1.,0.,0.));
#3320=DIRECTION('center_axis',(0.,-1.,0.));
#3321=DIRECTION('ref_axis',(1.,0.,0.));
#3322=DIRECTION('',(0.707106781186547,0.707106781186548,8.65956056235493E-17));
#3323=DIRECTION('center_axis',(0.,-1.,0.));
#3324=DIRECTION('ref_axis',(1.,0.,0.));
#3325=DIRECTION('center_axis',(0.,-1.,0.));
#3326=DIRECTION('ref_axis',(1.,0.,0.));
#3327=DIRECTION('',(0.,1.,0.));
#3328=DIRECTION('center_axis',(0.,1.,0.));
#3329=DIRECTION('ref_axis',(1.,0.,0.));
#3330=DIRECTION('center_axis',(0.,-1.,0.));
#3331=DIRECTION('ref_axis',(1.,0.,0.));
#3332=DIRECTION('',(-0.707106781186547,0.707106781186548,-8.65956056235493E-17));
#3333=DIRECTION('center_axis',(0.,-1.,0.));
#3334=DIRECTION('ref_axis',(0.,0.,-1.));
#3335=DIRECTION('center_axis',(0.,-1.,0.));
#3336=DIRECTION('ref_axis',(1.,0.,0.));
#3337=DIRECTION('center_axis',(0.,1.,0.));
#3338=DIRECTION('ref_axis',(1.,0.,0.));
#3339=DIRECTION('center_axis',(0.,1.,0.));
#3340=DIRECTION('ref_axis',(1.,0.,0.));
#3341=DIRECTION('',(-0.447213595499958,0.894427190999916,-5.47678698264203E-17));
#3342=DIRECTION('center_axis',(0.,-1.,0.));
#3343=DIRECTION('ref_axis',(1.,0.,0.));
#3344=DIRECTION('',(0.,1.,0.));
#4055=CARTESIAN_POINT('',(0.,0.,0.));
#4056=CARTESIAN_POINT('Origin',(0.0866025403784439,-0.4,-0.15));
#4057=CARTESIAN_POINT('',(0.173205080756888,-0.4,0.));
#4058=CARTESIAN_POINT('',(0.0866025403784439,-0.4,-0.15));
#4059=CARTESIAN_POINT('',(0.173205080756888,-0.4,0.));
#4060=CARTESIAN_POINT('',(0.0866025403784439,-0.64,-0.15));
#4061=CARTESIAN_POINT('',(0.0866025403784439,-0.4,-0.15));
#4062=CARTESIAN_POINT('',(0.173205080756888,-0.64,0.));
#4063=CARTESIAN_POINT('',(0.173205080756888,-0.64,0.));
#4064=CARTESIAN_POINT('',(0.173205080756888,-0.4,0.));
#4065=CARTESIAN_POINT('Origin',(-0.0866025403784438,-0.4,-0.15));
#4066=CARTESIAN_POINT('',(-0.0866025403784438,-0.4,-0.15));
#4067=CARTESIAN_POINT('',(0.0866025403784439,-0.4,-0.15));
#4068=CARTESIAN_POINT('',(-0.0866025403784438,-0.64,-0.15));
#4069=CARTESIAN_POINT('',(-0.0866025403784438,-0.4,-0.15));
#4070=CARTESIAN_POINT('',(0.0866025403784439,-0.64,-0.15));
#4071=CARTESIAN_POINT('Origin',(-0.173205080756888,-0.4,-2.77555756156289E-17));
#4072=CARTESIAN_POINT('',(-0.173205080756888,-0.4,-2.12115047744981E-17));
#4073=CARTESIAN_POINT('',(-0.0866025403784438,-0.4,-0.15));
#4074=CARTESIAN_POINT('',(-0.173205080756888,-0.64,-2.77555756156289E-17));
#4075=CARTESIAN_POINT('',(-0.173205080756888,-0.4,-2.12115047744981E-17));
#4076=CARTESIAN_POINT('',(-0.0866025403784438,-0.64,-0.15));
#4077=CARTESIAN_POINT('Origin',(-0.0866025403784439,-0.4,0.15));
#4078=CARTESIAN_POINT('',(-0.0866025403784439,-0.4,0.15));
#4079=CARTESIAN_POINT('',(-0.173205080756888,-0.4,-2.12115047744981E-17));
#4080=CARTESIAN_POINT('',(-0.0866025403784439,-0.64,0.15));
#4081=CARTESIAN_POINT('',(-0.0866025403784439,-0.4,0.15));
#4082=CARTESIAN_POINT('',(-0.173205080756888,-0.64,-2.12115047744981E-17));
#4083=CARTESIAN_POINT('Origin',(0.0866025403784439,-0.4,0.15));
#4084=CARTESIAN_POINT('',(0.0866025403784439,-0.4,0.15));
#4085=CARTESIAN_POINT('',(-0.0866025403784439,-0.4,0.15));
#4086=CARTESIAN_POINT('',(0.0866025403784439,-0.64,0.15));
#4087=CARTESIAN_POINT('',(0.0866025403784439,-0.4,0.15));
#4088=CARTESIAN_POINT('',(-0.0866025403784439,-0.64,0.15));
#4089=CARTESIAN_POINT('Origin',(0.173205080756888,-0.4,0.));
#4090=CARTESIAN_POINT('',(0.0866025403784439,-0.4,0.15));
#4091=CARTESIAN_POINT('',(0.0866025403784439,-0.64,0.15));
#4092=CARTESIAN_POINT('Origin',(0.,-0.4,-2.77555756156289E-17));
#4093=CARTESIAN_POINT('Origin',(0.,-0.64,-2.77555756156289E-17));
#4094=CARTESIAN_POINT('Origin',(0.,-1.,0.));
#4095=CARTESIAN_POINT('',(-0.1954,-1.,2.39295984553393E-17));
#4096=CARTESIAN_POINT('Origin',(0.,-1.,0.));
#4097=CARTESIAN_POINT('Origin',(0.3,0.4,0.));
#4098=CARTESIAN_POINT('',(-0.3,0.4,-3.67394039744206E-17));
#4099=CARTESIAN_POINT('Origin',(0.,0.4,0.));
#4100=CARTESIAN_POINT('Origin',(0.,0.375,0.));
#4101=CARTESIAN_POINT('',(-0.35,0.35,-4.28626379701573E-17));
#4102=CARTESIAN_POINT('Origin',(0.,0.35,0.));
#4103=CARTESIAN_POINT('',(-0.325,0.375,-3.9801020972289E-17));
#4104=CARTESIAN_POINT('Origin',(0.,0.19,0.));
#4105=CARTESIAN_POINT('',(-0.35,0.03,-4.28626379701574E-17));
#4106=CARTESIAN_POINT('Origin',(0.,0.03,0.));
#4107=CARTESIAN_POINT('',(-0.35,0.19,-4.28626379701574E-17));
#4108=CARTESIAN_POINT('Origin',(0.,0.0149999999999999,0.));
#4109=CARTESIAN_POINT('',(-0.32,-3.29597460435593E-17,-3.91886975727153E-17));
#4110=CARTESIAN_POINT('Origin',(0.,0.,0.));
#4111=CARTESIAN_POINT('',(-0.335,0.0149999999999999,-4.10256677714363E-17));
#4112=CARTESIAN_POINT('Origin',(0.22,0.,0.));
#4113=CARTESIAN_POINT('',(-0.22,-6.93889390390723E-18,-2.69422295812418E-17));
#4114=CARTESIAN_POINT('Origin',(0.,0.,0.));
#4115=CARTESIAN_POINT('Origin',(0.,-0.02,0.));
#4116=CARTESIAN_POINT('',(-0.1954,-0.0492,2.39295984553393E-17));
#4117=CARTESIAN_POINT('Origin',(0.,-0.0492,0.));
#4118=CARTESIAN_POINT('',(-0.21,-0.02,-2.57175827820944E-17));
#4119=CARTESIAN_POINT('Origin',(0.,-0.8,0.));
#4120=CARTESIAN_POINT('',(-0.1954,-0.8,-2.39295984553393E-17));
#4745=UNCERTAINTY_MEASURE_WITH_UNIT(LENGTH_MEASURE(0.001),#4778,
'DISTANCE_ACCURACY_VALUE',
'Maximum model space distance between geometric entities at asserted c
onnectivities');
#4755=UNCERTAINTY_MEASURE_WITH_UNIT(LENGTH_MEASURE(0.001),#4778,
'DISTANCE_ACCURACY_VALUE',
'Maximum model space distance between geometric entities at asserted c
onnectivities');
#4767=(
GEOMETRIC_REPRESENTATION_CONTEXT(3)
GLOBAL_UNCERTAINTY_ASSIGNED_CONTEXT((#4745))
GLOBAL_UNIT_ASSIGNED_CONTEXT((#4778,#4780,#4781))
REPRESENTATION_CONTEXT('','3D')
);
#4777=(
GEOMETRIC_REPRESENTATION_CONTEXT(3)
GLOBAL_UNCERTAINTY_ASSIGNED_CONTEXT((#4755))
GLOBAL_UNIT_ASSIGNED_CONTEXT((#4778,#4780,#4781))
REPRESENTATION_CONTEXT('','3D')
);
#4778=(
LENGTH_UNIT()
NAMED_UNIT(*)
SI_UNIT(.CENTI.,.METRE.)
);
#4780=(
NAMED_UNIT(*)
PLANE_ANGLE_UNIT()
SI_UNIT($,.RADIAN.)
);
#4781=(
NAMED_UNIT(*)
SI_UNIT($,.STERADIAN.)
SOLID_ANGLE_UNIT()
);
#4793=SHAPE_DEFINITION_REPRESENTATION(#4814,#4882);
#4814=PRODUCT_DEFINITION_SHAPE('',$,#4904);
#4882=SHAPE_REPRESENTATION('',(#2711),#4767);
#4892=PRODUCT_DEFINITION_CONTEXT('part definition',#4957,'design');
#4904=PRODUCT_DEFINITION('M4x10 Cap Screw','M4x10 Cap Screw',#4925,#4892);
#4925=PRODUCT_DEFINITION_FORMATION('',$,#4970);
#4957=APPLICATION_CONTEXT(
'Core Data for Automotive Mechanical Design Process');
#4958=PRODUCT_CONTEXT('part definition',#4957,'mechanical');
#4970=PRODUCT('M4x10 Cap Screw','M4x10 Cap Screw','M4x10 Cap Screw',(#4958));
#5057=COLOUR_RGB('Black',0.12,0.14,0.17);
#5058=FILL_AREA_STYLE_COLOUR('',#5057);
#5059=FILL_AREA_STYLE('',(#5058));
#5060=SURFACE_STYLE_FILL_AREA(#5059);
#5061=SURFACE_SIDE_STYLE('',(#5060));
#5062=SURFACE_STYLE_USAGE(.BOTH.,#5061);
#5063=PRESENTATION_STYLE_ASSIGNMENT((#5062));
ENDSEC;
END-ISO-10303-21;
